ISO-10303-21;
HEADER;
/* Generated by software containing ST-Developer
 * from STEP Tools, Inc. (www.steptools.com) 
 */

FILE_DESCRIPTION(
/* description */ ('Indexing fixture plate with plunger'),
/* implementation_level */ '2;1');

FILE_NAME(
/* name */ 'M5x5 collar screw.step',
/* time_stamp */ '2026-10-28T03:23:41-07:00',
/* author */ (''),
/* organization */ (''),
/* preprocessor_version */ 'ST-DEVELOPER v20.2',
/* originating_system */ 'Autodesk Translation Framework v15.17.0.0',
/* authorisation */ '');

FILE_SCHEMA (('AUTOMOTIVE_DESIGN { 1 0 10303 214 3 1 1 }'));
ENDSEC;

DATA;
#10=MECHANICAL_DESIGN_GEOMETRIC_PRESENTATION_REPRESENTATION('',(#344),#10020);
#222=CONICAL_SURFACE('',#5240,0.235,0.785398163397448);
#281=SHAPE_REPRESENTATION_RELATIONSHIP('SRR','None',#10156,#308);
#308=ADVANCED_BREP_SHAPE_REPRESENTATION('',(#379),#10009);
#344=STYLED_ITEM('',(#10375),#379);
#379=MANIFOLD_SOLID_BREP('Body1',#4599);
#440=FACE_BOUND('',#1158,.T.);
#601=PLANE('',#5229);
#602=PLANE('',#5231);
#603=PLANE('',#5232);
#604=PLANE('',#5233);
#605=PLANE('',#5234);
#606=PLANE('',#5235);
#607=PLANE('',#5236);
#608=PLANE('',#5237);
#609=PLANE('',#5238);
#810=FACE_OUTER_BOUND('',#1149,.T.);
#811=FACE_OUTER_BOUND('',#1150,.T.);
#812=FACE_OUTER_BOUND('',#1151,.T.);
#813=FACE_OUTER_BOUND('',#1152,.T.);
#814=FACE_OUTER_BOUND('',#1153,.T.);
#815=FACE_OUTER_BOUND('',#1154,.T.);
#816=FACE_OUTER_BOUND('',#1155,.T.);
#817=FACE_OUTER_BOUND('',#1156,.T.);
#818=FACE_OUTER_BOUND('',#1157,.T.);
#819=FACE_OUTER_BOUND('',#1159,.T.);
#820=FACE_OUTER_BOUND('',#1160,.T.);
#1149=EDGE_LOOP('',(#3597));
#1150=EDGE_LOOP('',(#3598,#3599,#3600,#3601));
#1151=EDGE_LOOP('',(#3602,#3603,#3604,#3605));
#1152=EDGE_LOOP('',(#3606,#3607,#3608,#3609));
#1153=EDGE_LOOP('',(#3610,#3611,#3612,#3613));
#1154=EDGE_LOOP('',(#3614,#3615,#3616,#3617));
#1155=EDGE_LOOP('',(#3618,#3619,#3620,#3621));
#1156=EDGE_LOOP('',(#3622,#3623,#3624,#3625,#3626,#3627));
#1157=EDGE_LOOP('',(#3628));
#1158=EDGE_LOOP('',(#3629,#3630,#3631,#3632,#3633,#3634));
#1159=EDGE_LOOP('',(#3635,#3636,#3637,#3638));
#1160=EDGE_LOOP('',(#3639,#3640,#3641,#3642));
#1479=LINE('',#9246,#1699);
#1480=LINE('',#9248,#1700);
#1481=LINE('',#9250,#1701);
#1482=LINE('',#9251,#1702);
#1483=LINE('',#9254,#1703);
#1484=LINE('',#9256,#1704);
#1485=LINE('',#9257,#1705);
#1486=LINE('',#9260,#1706);
#1487=LINE('',#9262,#1707);
#1488=LINE('',#9263,#1708);
#1489=LINE('',#9266,#1709);
#1490=LINE('',#9268,#1710);
#1491=LINE('',#9269,#1711);
#1492=LINE('',#9272,#1712);
#1493=LINE('',#9274,#1713);
#1494=LINE('',#9275,#1714);
#1495=LINE('',#9277,#1715);
#1496=LINE('',#9278,#1716);
#1497=LINE('',#9286,#1717);
#1498=LINE('',#9288,#1718);
#1699=VECTOR('',#6310,1.);
#1700=VECTOR('',#6311,1.);
#1701=VECTOR('',#6312,1.);
#1702=VECTOR('',#6313,1.);
#1703=VECTOR('',#6316,1.);
#1704=VECTOR('',#6317,1.);
#1705=VECTOR('',#6318,1.);
#1706=VECTOR('',#6321,1.);
#1707=VECTOR('',#6322,1.);
#1708=VECTOR('',#6323,1.);
#1709=VECTOR('',#6326,1.);
#1710=VECTOR('',#6327,1.);
#1711=VECTOR('',#6328,1.);
#1712=VECTOR('',#6331,1.);
#1713=VECTOR('',#6332,1.);
#1714=VECTOR('',#6333,1.);
#1715=VECTOR('',#6336,1.);
#1716=VECTOR('',#6337,1.);
#1717=VECTOR('',#6348,0.235);
#1718=VECTOR('',#6351,0.25);
#1988=CIRCLE('',#5230,0.24505);
#1989=CIRCLE('',#5239,0.22);
#1990=CIRCLE('',#5241,0.24505);
#2323=VERTEX_POINT('',#9241);
#2324=VERTEX_POINT('',#9244);
#2325=VERTEX_POINT('',#9245);
#2326=VERTEX_POINT('',#9247);
#2327=VERTEX_POINT('',#9249);
#2328=VERTEX_POINT('',#9253);
#2329=VERTEX_POINT('',#9255);
#2330=VERTEX_POINT('',#9259);
#2331=VERTEX_POINT('',#9261);
#2332=VERTEX_POINT('',#9265);
#2333=VERTEX_POINT('',#9267);
#2334=VERTEX_POINT('',#9271);
#2335=VERTEX_POINT('',#9273);
#2336=VERTEX_POINT('',#9281);
#2337=VERTEX_POINT('',#9284);
#2778=EDGE_CURVE('',#2323,#2323,#1988,.T.);
#2779=EDGE_CURVE('',#2324,#2325,#1479,.T.);
#2780=EDGE_CURVE('',#2324,#2326,#1480,.T.);
#2781=EDGE_CURVE('',#2326,#2327,#1481,.T.);
#2782=EDGE_CURVE('',#2325,#2327,#1482,.T.);
#2783=EDGE_CURVE('',#2328,#2324,#1483,.T.);
#2784=EDGE_CURVE('',#2328,#2329,#1484,.T.);
#2785=EDGE_CURVE('',#2329,#2326,#1485,.T.);
#2786=EDGE_CURVE('',#2330,#2328,#1486,.T.);
#2787=EDGE_CURVE('',#2330,#2331,#1487,.T.);
#2788=EDGE_CURVE('',#2331,#2329,#1488,.T.);
#2789=EDGE_CURVE('',#2332,#2330,#1489,.T.);
#2790=EDGE_CURVE('',#2332,#2333,#1490,.T.);
#2791=EDGE_CURVE('',#2333,#2331,#1491,.T.);
#2792=EDGE_CURVE('',#2334,#2332,#1492,.T.);
#2793=EDGE_CURVE('',#2334,#2335,#1493,.T.);
#2794=EDGE_CURVE('',#2335,#2333,#1494,.T.);
#2795=EDGE_CURVE('',#2325,#2334,#1495,.T.);
#2796=EDGE_CURVE('',#2327,#2335,#1496,.T.);
#2797=EDGE_CURVE('',#2336,#2336,#1989,.T.);
#2798=EDGE_CURVE('',#2337,#2337,#1990,.T.);
#2799=EDGE_CURVE('',#2337,#2336,#1497,.T.);
#2800=EDGE_CURVE('',#2323,#2337,#1498,.T.);
#3597=ORIENTED_EDGE('',*,*,#2778,.F.);
#3598=ORIENTED_EDGE('',*,*,#2779,.F.);
#3599=ORIENTED_EDGE('',*,*,#2780,.T.);
#3600=ORIENTED_EDGE('',*,*,#2781,.T.);
#3601=ORIENTED_EDGE('',*,*,#2782,.F.);
#3602=ORIENTED_EDGE('',*,*,#2783,.F.);
#3603=ORIENTED_EDGE('',*,*,#2784,.T.);
#3604=ORIENTED_EDGE('',*,*,#2785,.T.);
#3605=ORIENTED_EDGE('',*,*,#2780,.F.);
#3606=ORIENTED_EDGE('',*,*,#2786,.F.);
#3607=ORIENTED_EDGE('',*,*,#2787,.T.);
#3608=ORIENTED_EDGE('',*,*,#2788,.T.);
#3609=ORIENTED_EDGE('',*,*,#2784,.F.);
#3610=ORIENTED_EDGE('',*,*,#2789,.F.);
#3611=ORIENTED_EDGE('',*,*,#2790,.T.);
#3612=ORIENTED_EDGE('',*,*,#2791,.T.);
#3613=ORIENTED_EDGE('',*,*,#2787,.F.);
#3614=ORIENTED_EDGE('',*,*,#2792,.F.);
#3615=ORIENTED_EDGE('',*,*,#2793,.T.);
#3616=ORIENTED_EDGE('',*,*,#2794,.T.);
#3617=ORIENTED_EDGE('',*,*,#2790,.F.);
#3618=ORIENTED_EDGE('',*,*,#2795,.F.);
#3619=ORIENTED_EDGE('',*,*,#2782,.T.);
#3620=ORIENTED_EDGE('',*,*,#2796,.T.);
#3621=ORIENTED_EDGE('',*,*,#2793,.F.);
#3622=ORIENTED_EDGE('',*,*,#2796,.F.);
#3623=ORIENTED_EDGE('',*,*,#2781,.F.);
#3624=ORIENTED_EDGE('',*,*,#2785,.F.);
#3625=ORIENTED_EDGE('',*,*,#2788,.F.);
#3626=ORIENTED_EDGE('',*,*,#2791,.F.);
#3627=ORIENTED_EDGE('',*,*,#2794,.F.);
#3628=ORIENTED_EDGE('',*,*,#2797,.F.);
#3629=ORIENTED_EDGE('',*,*,#2779,.T.);
#3630=ORIENTED_EDGE('',*,*,#2795,.T.);
#3631=ORIENTED_EDGE('',*,*,#2792,.T.);
#3632=ORIENTED_EDGE('',*,*,#2789,.T.);
#3633=ORIENTED_EDGE('',*,*,#2786,.T.);
#3634=ORIENTED_EDGE('',*,*,#2783,.T.);
#3635=ORIENTED_EDGE('',*,*,#2798,.F.);
#3636=ORIENTED_EDGE('',*,*,#2799,.T.);
#3637=ORIENTED_EDGE('',*,*,#2797,.T.);
#3638=ORIENTED_EDGE('',*,*,#2799,.F.);
#3639=ORIENTED_EDGE('',*,*,#2778,.T.);
#3640=ORIENTED_EDGE('',*,*,#2800,.T.);
#3641=ORIENTED_EDGE('',*,*,#2798,.T.);
#3642=ORIENTED_EDGE('',*,*,#2800,.F.);
#4215=CYLINDRICAL_SURFACE('',#5242,0.24505);
#4425=ADVANCED_FACE('',(#810),#601,.F.);
#4426=ADVANCED_FACE('',(#811),#602,.F.);
#4427=ADVANCED_FACE('',(#812),#603,.F.);
#4428=ADVANCED_FACE('',(#813),#604,.F.);
#4429=ADVANCED_FACE('',(#814),#605,.F.);
#4430=ADVANCED_FACE('',(#815),#606,.F.);
#4431=ADVANCED_FACE('',(#816),#607,.F.);
#4432=ADVANCED_FACE('',(#817),#608,.F.);
#4433=ADVANCED_FACE('',(#818,#440),#609,.T.);
#4434=ADVANCED_FACE('',(#819),#222,.T.);
#4435=ADVANCED_FACE('',(#820),#4215,.T.);
#4599=CLOSED_SHELL('',(#4425,#4426,#4427,#4428,#4429,#4430,#4431,#4432,
#4433,#4434,#4435));
#5228=AXIS2_PLACEMENT_3D('',#9239,#6302,#6303);
#5229=AXIS2_PLACEMENT_3D('',#9240,#6304,#6305);
#5230=AXIS2_PLACEMENT_3D('',#9242,#6306,#6307);
#5231=AXIS2_PLACEMENT_3D('',#9243,#6308,#6309);
#5232=AXIS2_PLACEMENT_3D('',#9252,#6314,#6315);
#5233=AXIS2_PLACEMENT_3D('',#9258,#6319,#6320);
#5234=AXIS2_PLACEMENT_3D('',#9264,#6324,#6325);
#5235=AXIS2_PLACEMENT_3D('',#9270,#6329,#6330);
#5236=AXIS2_PLACEMENT_3D('',#9276,#6334,#6335);
#5237=AXIS2_PLACEMENT_3D('',#9279,#6338,#6339);
#5238=AXIS2_PLACEMENT_3D('',#9280,#6340,#6341);
#5239=AXIS2_PLACEMENT_3D('',#9282,#6342,#6343);
#5240=AXIS2_PLACEMENT_3D('',#9283,#6344,#6345);
#5241=AXIS2_PLACEMENT_3D('',#9285,#6346,#6347);
#5242=AXIS2_PLACEMENT_3D('',#9287,#6349,#6350);
#6302=DIRECTION('axis',(0.,0.,1.));
#6303=DIRECTION('refdir',(1.,0.,0.));
#6304=DIRECTION('center_axis',(0.,1.,0.));
#6305=DIRECTION('ref_axis',(1.,0.,0.));
#6306=DIRECTION('center_axis',(0.,1.,0.));
#6307=DIRECTION('ref_axis',(1.,0.,0.));
#6308=DIRECTION('center_axis',(0.866025403784439,0.,-0.5));
#6309=DIRECTION('ref_axis',(0.5,0.,0.866025403784439));
#6310=DIRECTION('',(0.5,0.,0.866025403784439));
#6311=DIRECTION('',(0.,-1.,0.));
#6312=DIRECTION('',(0.5,0.,0.866025403784439));
#6313=DIRECTION('',(0.,-1.,0.));
#6314=DIRECTION('center_axis',(1.92296268638356E-16,0.,-1.));
#6315=DIRECTION('ref_axis',(1.,0.,1.92296268638356E-16));
#6316=DIRECTION('',(1.,0.,1.92296268638356E-16));
#6317=DIRECTION('',(0.,-1.,0.));
#6318=DIRECTION('',(1.,0.,1.92296268638356E-16));
#6319=DIRECTION('center_axis',(-0.866025403784439,0.,-0.5));
#6320=DIRECTION('ref_axis',(0.5,0.,-0.866025403784439));
#6321=DIRECTION('',(0.5,0.,-0.866025403784439));
#6322=DIRECTION('',(0.,-1.,0.));
#6323=DIRECTION('',(0.5,0.,-0.866025403784438));
#6324=DIRECTION('center_axis',(-0.866025403784439,0.,0.5));
#6325=DIRECTION('ref_axis',(-0.5,0.,-0.866025403784439));
#6326=DIRECTION('',(-0.5,0.,-0.866025403784439));
#6327=DIRECTION('',(0.,-1.,0.));
#6328=DIRECTION('',(-0.5,0.,-0.866025403784439));
#6329=DIRECTION('center_axis',(-1.92296268638356E-16,0.,1.));
#6330=DIRECTION('ref_axis',(-1.,0.,-1.92296268638356E-16));
#6331=DIRECTION('',(-1.,0.,-1.92296268638356E-16));
#6332=DIRECTION('',(0.,-1.,0.));
#6333=DIRECTION('',(-1.,0.,-1.92296268638356E-16));
#6334=DIRECTION('center_axis',(0.866025403784439,0.,0.5));
#6335=DIRECTION('ref_axis',(-0.5,0.,0.866025403784439));
#6336=DIRECTION('',(-0.5,0.,0.866025403784439));
#6337=DIRECTION('',(-0.5,0.,0.866025403784439));
#6338=DIRECTION('center_axis',(0.,-1.,0.));
#6339=DIRECTION('ref_axis',(0.,0.,-1.));
#6340=DIRECTION('center_axis',(0.,1.,0.));
#6341=DIRECTION('ref_axis',(0.,0.,1.));
#6342=DIRECTION('center_axis',(0.,-1.,0.));
#6343=DIRECTION('ref_axis',(1.,0.,0.));
#6344=DIRECTION('center_axis',(0.,-1.,0.));
#6345=DIRECTION('ref_axis',(1.,0.,0.));
#6346=DIRECTION('center_axis',(0.,-1.,0.));
#6347=DIRECTION('ref_axis',(1.,0.,0.));
#6348=DIRECTION('',(0.707106781186547,0.707106781186548,8.65956056235493E-17));
#6349=DIRECTION('center_axis',(0.,-1.,0.));
#6350=DIRECTION('ref_axis',(1.,0.,0.));
#6351=DIRECTION('',(0.,1.,0.));
#9239=CARTESIAN_POINT('',(0.,0.,0.));
#9240=CARTESIAN_POINT('Origin',(0.,-0.5,0.));
#9241=CARTESIAN_POINT('',(-0.24505,-0.5,3.00099698131059E-17));
#9242=CARTESIAN_POINT('Origin',(0.,-0.5,0.));
#9243=CARTESIAN_POINT('Origin',(0.0721687836487032,0.,-0.125));
#9244=CARTESIAN_POINT('',(0.0721687836487032,0.,-0.125));
#9245=CARTESIAN_POINT('',(0.144337567297406,0.,0.));
#9246=CARTESIAN_POINT('',(0.117710979560879,0.,-0.0461186027918559));
#9247=CARTESIAN_POINT('',(0.0721687836487032,-0.25,-0.125));
#9248=CARTESIAN_POINT('',(0.0721687836487032,0.,-0.125));
#9249=CARTESIAN_POINT('',(0.144337567297406,-0.25,0.));
#9250=CARTESIAN_POINT('',(0.144337567297406,-0.25,0.));
#9251=CARTESIAN_POINT('',(0.144337567297406,0.,0.));
#9252=CARTESIAN_POINT('Origin',(-0.0721687836487032,0.,-0.125));
#9253=CARTESIAN_POINT('',(-0.0721687836487032,0.,-0.125));
#9254=CARTESIAN_POINT('',(0.0739156081756484,0.,-0.125));
#9255=CARTESIAN_POINT('',(-0.0721687836487032,-0.25,-0.125));
#9256=CARTESIAN_POINT('',(-0.0721687836487032,0.,-0.125));
#9257=CARTESIAN_POINT('',(0.0721687836487032,-0.25,-0.125));
#9258=CARTESIAN_POINT('Origin',(-0.144337567297406,0.,-4.16333634234434E-17));
#9259=CARTESIAN_POINT('',(-0.144337567297406,0.,-1.76762539787485E-17));
#9260=CARTESIAN_POINT('',(-0.0987953713852306,0.,-0.0788813972081442));
#9261=CARTESIAN_POINT('',(-0.144337567297406,-0.25,-2.77555756156289E-17));
#9262=CARTESIAN_POINT('',(-0.144337567297406,0.,-1.76762539787485E-17));
#9263=CARTESIAN_POINT('',(-0.0721687836487032,-0.25,-0.125));
#9264=CARTESIAN_POINT('Origin',(-0.0721687836487033,0.,0.125));
#9265=CARTESIAN_POINT('',(-0.0721687836487033,0.,0.125));
#9266=CARTESIAN_POINT('',(-0.0627109795608791,0.,0.141381397208144));
#9267=CARTESIAN_POINT('',(-0.0721687836487033,-0.25,0.125));
#9268=CARTESIAN_POINT('',(-0.0721687836487033,0.,0.125));
#9269=CARTESIAN_POINT('',(-0.144337567297406,-0.25,-1.76762539787485E-17));
#9270=CARTESIAN_POINT('Origin',(0.0721687836487032,0.,0.125));
#9271=CARTESIAN_POINT('',(0.0721687836487032,0.,0.125));
#9272=CARTESIAN_POINT('',(0.146084391824352,0.,0.125));
#9273=CARTESIAN_POINT('',(0.0721687836487032,-0.25,0.125));
#9274=CARTESIAN_POINT('',(0.0721687836487032,0.,0.125));
#9275=CARTESIAN_POINT('',(-0.0721687836487033,-0.25,0.125));
#9276=CARTESIAN_POINT('Origin',(0.144337567297406,0.,0.));
#9277=CARTESIAN_POINT('',(0.153795371385231,0.,-0.0163813972081441));
#9278=CARTESIAN_POINT('',(0.0721687836487032,-0.25,0.125));
#9279=CARTESIAN_POINT('Origin',(0.,-0.25,0.));
#9280=CARTESIAN_POINT('Origin',(0.22,0.,0.));
#9281=CARTESIAN_POINT('',(-0.22,-8.67361737988404E-18,-2.69422295812418E-17));
#9282=CARTESIAN_POINT('Origin',(0.,0.,0.));
#9283=CARTESIAN_POINT('Origin',(0.,-0.015,0.));
#9284=CARTESIAN_POINT('',(-0.24505,-0.02505,-3.00099698131059E-17));
#9285=CARTESIAN_POINT('Origin',(0.,-0.02505,0.));
#9286=CARTESIAN_POINT('',(-0.235,-0.015,-2.87791997799628E-17));
#9287=CARTESIAN_POINT('Origin',(0.,-0.3775,0.));
#9288=CARTESIAN_POINT('',(-0.24505,-0.3775,-3.00099698131059E-17));
#9976=UNCERTAINTY_MEASURE_WITH_UNIT(LENGTH_MEASURE(0.001),#10021,
'DISTANCE_ACCURACY_VALUE',
'Maximum model space distance between geometric entities at asserted c
onnectivities');
#9987=UNCERTAINTY_MEASURE_WITH_UNIT(LENGTH_MEASURE(0.001),#10021,
'DISTANCE_ACCURACY_VALUE',
'Maximum model space distance between geometric entities at asserted c
onnectivities');
#10009=(
GEOMETRIC_REPRESENTATION_CONTEXT(3)
GLOBAL_UNCERTAINTY_ASSIGNED_CONTEXT((#9976))
GLOBAL_UNIT_ASSIGNED_CONTEXT((#10021,#10023,#10024))
REPRESENTATION_CONTEXT('','3D')
);
#10020=(
GEOMETRIC_REPRESENTATION_CONTEXT(3)
GLOBAL_UNCERTAINTY_ASSIGNED_CONTEXT((#9987))
GLOBAL_UNIT_ASSIGNED_CONTEXT((#10021,#10023,#10024))
REPRESENTATION_CONTEXT('','3D')
);
#10021=(
LENGTH_UNIT()
NAMED_UNIT(*)
SI_UNIT(.CENTI.,.METRE.)
);
#10023=(
NAMED_UNIT(*)
PLANE_ANGLE_UNIT()
SI_UNIT($,.RADIAN.)
);
#10024=(
NAMED_UNIT(*)
SI_UNIT($,.STERADIAN.)
SOLID_ANGLE_UNIT()
);
#10046=SHAPE_DEFINITION_REPRESENTATION(#10083,#10156);
#10083=PRODUCT_DEFINITION_SHAPE('',$,#10189);
#10156=SHAPE_REPRESENTATION('',(#5228),#10009);
#10167=PRODUCT_DEFINITION_CONTEXT('part definition',#10265,'design');
#10189=PRODUCT_DEFINITION('M5x5 collar screw','M5x5 collar screw',#10221,
#10167);
#10221=PRODUCT_DEFINITION_FORMATION('',$,#10288);
#10265=APPLICATION_CONTEXT(
'Core Data for Automotive Mechanical Design Process');
#10266=PRODUCT_CONTEXT('part definition',#10265,'mechanical');
#10288=PRODUCT('M5x5 collar screw','M5x5 collar screw',
'M5x5 collar screw',(#10266));
#10369=COLOUR_RGB('Black',0.12,0.14,0.17);
#10370=FILL_AREA_STYLE_COLOUR('',#10369);
#10371=FILL_AREA_STYLE('',(#10370));
#10372=SURFACE_STYLE_FILL_AREA(#10371);
#10373=SURFACE_SIDE_STYLE('',(#10372));
#10374=SURFACE_STYLE_USAGE(.BOTH.,#10373);
#10375=PRESENTATION_STYLE_ASSIGNMENT((#10374));
ENDSEC;
END-ISO-10303-21;
